ISO-10303-21;
HEADER;
/* Generated by software containing ST-Developer
 * from STEP Tools, Inc. (www.steptools.com) 
 */

FILE_DESCRIPTION(
/* description */ ('Shaft runout checking stand'),
/* implementation_level */ '2;1');

FILE_NAME(
/* name */ 'Dead axle (3).step',
/* time_stamp */ '2026-11-02T21:12:33-08:00',
/* author */ (''),
/* organization */ (''),
/* preprocessor_version */ 'ST-DEVELOPER v20.2',
/* originating_system */ 'Autodesk Translation Framework v15.17.0.0',
/* authorisation */ '');

FILE_SCHEMA (('AUTOMOTIVE_DESIGN { 1 0 10303 214 3 1 1 }'));
ENDSEC;

DATA;
#10=MECHANICAL_DESIGN_GEOMETRIC_PRESENTATION_REPRESENTATION('',(#482),#11748);
#396=SHAPE_REPRESENTATION_RELATIONSHIP('SRR','None',#11945,#439);
#439=ADVANCED_BREP_SHAPE_REPRESENTATION('',(#532),#11721);
#482=STYLED_ITEM('',(#12169),#532);
#532=MANIFOLD_SOLID_BREP('Body1',#6226);
#628=FACE_BOUND('',#1664,.T.);
#629=FACE_BOUND('',#1669,.T.);
#781=CIRCLE('',#7056,0.165);
#782=CIRCLE('',#7057,0.165);
#783=CIRCLE('',#7060,0.8);
#784=CIRCLE('',#7061,0.5);
#785=CIRCLE('',#7063,0.8);
#786=CIRCLE('',#7066,0.5);
#989=CYLINDRICAL_SURFACE('',#7055,0.165);
#990=CYLINDRICAL_SURFACE('',#7062,0.8);
#991=CYLINDRICAL_SURFACE('',#7065,0.5);
#1227=FACE_OUTER_BOUND('',#1661,.T.);
#1228=FACE_OUTER_BOUND('',#1662,.T.);
#1229=FACE_OUTER_BOUND('',#1663,.T.);
#1230=FACE_OUTER_BOUND('',#1665,.T.);
#1231=FACE_OUTER_BOUND('',#1666,.T.);
#1232=FACE_OUTER_BOUND('',#1667,.T.);
#1233=FACE_OUTER_BOUND('',#1668,.T.);
#1661=EDGE_LOOP('',(#4938,#4939,#4940,#4941));
#1662=EDGE_LOOP('',(#4942));
#1663=EDGE_LOOP('',(#4943));
#1664=EDGE_LOOP('',(#4944));
#1665=EDGE_LOOP('',(#4945,#4946,#4947,#4948));
#1666=EDGE_LOOP('',(#4949));
#1667=EDGE_LOOP('',(#4950,#4951,#4952,#4953));
#1668=EDGE_LOOP('',(#4954));
#1669=EDGE_LOOP('',(#4955));
#2200=LINE('',#10397,#2667);
#2201=LINE('',#10407,#2668);
#2202=LINE('',#10413,#2669);
#2667=VECTOR('',#8453,0.165);
#2668=VECTOR('',#8466,0.8);
#2669=VECTOR('',#8475,0.5);
#3101=VERTEX_POINT('',#10394);
#3102=VERTEX_POINT('',#10396);
#3103=VERTEX_POINT('',#10401);
#3104=VERTEX_POINT('',#10403);
#3105=VERTEX_POINT('',#10406);
#3106=VERTEX_POINT('',#10411);
#3755=EDGE_CURVE('',#3101,#3101,#781,.T.);
#3756=EDGE_CURVE('',#3101,#3102,#2200,.T.);
#3757=EDGE_CURVE('',#3102,#3102,#782,.T.);
#3758=EDGE_CURVE('',#3103,#3103,#783,.T.);
#3759=EDGE_CURVE('',#3104,#3104,#784,.T.);
#3760=EDGE_CURVE('',#3103,#3105,#2201,.T.);
#3761=EDGE_CURVE('',#3105,#3105,#785,.T.);
#3762=EDGE_CURVE('',#3106,#3106,#786,.T.);
#3763=EDGE_CURVE('',#3106,#3104,#2202,.T.);
#4938=ORIENTED_EDGE('',*,*,#3755,.F.);
#4939=ORIENTED_EDGE('',*,*,#3756,.T.);
#4940=ORIENTED_EDGE('',*,*,#3757,.F.);
#4941=ORIENTED_EDGE('',*,*,#3756,.F.);
#4942=ORIENTED_EDGE('',*,*,#3755,.T.);
#4943=ORIENTED_EDGE('',*,*,#3758,.T.);
#4944=ORIENTED_EDGE('',*,*,#3759,.F.);
#4945=ORIENTED_EDGE('',*,*,#3758,.F.);
#4946=ORIENTED_EDGE('',*,*,#3760,.T.);
#4947=ORIENTED_EDGE('',*,*,#3761,.T.);
#4948=ORIENTED_EDGE('',*,*,#3760,.F.);
#4949=ORIENTED_EDGE('',*,*,#3761,.F.);
#4950=ORIENTED_EDGE('',*,*,#3762,.F.);
#4951=ORIENTED_EDGE('',*,*,#3763,.T.);
#4952=ORIENTED_EDGE('',*,*,#3759,.T.);
#4953=ORIENTED_EDGE('',*,*,#3763,.F.);
#4954=ORIENTED_EDGE('',*,*,#3762,.T.);
#4955=ORIENTED_EDGE('',*,*,#3757,.T.);
#5738=PLANE('',#7058);
#5739=PLANE('',#7059);
#5740=PLANE('',#7064);
#5741=PLANE('',#7067);
#6027=ADVANCED_FACE('',(#1227),#989,.F.);
#6028=ADVANCED_FACE('',(#1228),#5738,.T.);
#6029=ADVANCED_FACE('',(#1229,#628),#5739,.T.);
#6030=ADVANCED_FACE('',(#1230),#990,.T.);
#6031=ADVANCED_FACE('',(#1231),#5740,.F.);
#6032=ADVANCED_FACE('',(#1232),#991,.T.);
#6033=ADVANCED_FACE('',(#1233,#629),#5741,.T.);
#6226=CLOSED_SHELL('',(#6027,#6028,#6029,#6030,#6031,#6032,#6033));
#7054=AXIS2_PLACEMENT_3D('',#10392,#8447,#8448);
#7055=AXIS2_PLACEMENT_3D('',#10393,#8449,#8450);
#7056=AXIS2_PLACEMENT_3D('',#10395,#8451,#8452);
#7057=AXIS2_PLACEMENT_3D('',#10398,#8454,#8455);
#7058=AXIS2_PLACEMENT_3D('',#10399,#8456,#8457);
#7059=AXIS2_PLACEMENT_3D('',#10400,#8458,#8459);
#7060=AXIS2_PLACEMENT_3D('',#10402,#8460,#8461);
#7061=AXIS2_PLACEMENT_3D('',#10404,#8462,#8463);
#7062=AXIS2_PLACEMENT_3D('',#10405,#8464,#8465);
#7063=AXIS2_PLACEMENT_3D('',#10408,#8467,#8468);
#7064=AXIS2_PLACEMENT_3D('',#10409,#8469,#8470);
#7065=AXIS2_PLACEMENT_3D('',#10410,#8471,#8472);
#7066=AXIS2_PLACEMENT_3D('',#10412,#8473,#8474);
#7067=AXIS2_PLACEMENT_3D('',#10414,#8476,#8477);
#8447=DIRECTION('axis',(0.,0.,1.));
#8448=DIRECTION('refdir',(1.,0.,0.));
#8449=DIRECTION('center_axis',(0.,1.,0.));
#8450=DIRECTION('ref_axis',(1.,0.,0.));
#8451=DIRECTION('center_axis',(0.,1.,0.));
#8452=DIRECTION('ref_axis',(1.,0.,0.));
#8453=DIRECTION('',(0.,1.,0.));
#8454=DIRECTION('center_axis',(0.,-1.,0.));
#8455=DIRECTION('ref_axis',(1.,0.,0.));
#8456=DIRECTION('center_axis',(0.,1.,0.));
#8457=DIRECTION('ref_axis',(1.,0.,0.));
#8458=DIRECTION('center_axis',(0.,1.,0.));
#8459=DIRECTION('ref_axis',(1.,0.,0.));
#8460=DIRECTION('center_axis',(0.,1.,0.));
#8461=DIRECTION('ref_axis',(1.,0.,0.));
#8462=DIRECTION('center_axis',(0.,1.,0.));
#8463=DIRECTION('ref_axis',(1.,0.,0.));
#8464=DIRECTION('center_axis',(0.,1.,0.));
#8465=DIRECTION('ref_axis',(1.,0.,0.));
#8466=DIRECTION('',(0.,-1.,0.));
#8467=DIRECTION('center_axis',(0.,1.,0.));
#8468=DIRECTION('ref_axis',(1.,0.,0.));
#8469=DIRECTION('center_axis',(0.,1.,0.));
#8470=DIRECTION('ref_axis',(1.,0.,0.));
#8471=DIRECTION('center_axis',(0.,1.,0.));
#8472=DIRECTION('ref_axis',(1.,0.,0.));
#8473=DIRECTION('center_axis',(0.,1.,0.));
#8474=DIRECTION('ref_axis',(1.,0.,0.));
#8475=DIRECTION('',(0.,-1.,0.));
#8476=DIRECTION('center_axis',(0.,1.,0.));
#8477=DIRECTION('ref_axis',(1.,0.,0.));
#10392=CARTESIAN_POINT('',(0.,0.,0.));
#10393=CARTESIAN_POINT('Origin',(2.,9.6,5.));
#10394=CARTESIAN_POINT('',(1.835,9.6,5.));
#10395=CARTESIAN_POINT('Origin',(2.,9.6,5.));
#10396=CARTESIAN_POINT('',(1.835,10.8,5.));
#10397=CARTESIAN_POINT('',(1.835,9.6,5.));
#10398=CARTESIAN_POINT('Origin',(2.,10.8,5.));
#10399=CARTESIAN_POINT('Origin',(2.,9.6,5.));
#10400=CARTESIAN_POINT('Origin',(2.,8.5,5.));
#10401=CARTESIAN_POINT('',(1.2,8.5,5.));
#10402=CARTESIAN_POINT('Origin',(2.,8.5,5.));
#10403=CARTESIAN_POINT('',(1.5,8.5,5.));
#10404=CARTESIAN_POINT('Origin',(2.,8.5,5.));
#10405=CARTESIAN_POINT('Origin',(2.,8.2,5.));
#10406=CARTESIAN_POINT('',(1.2,8.2,5.));
#10407=CARTESIAN_POINT('',(1.2,8.2,5.));
#10408=CARTESIAN_POINT('Origin',(2.,8.2,5.));
#10409=CARTESIAN_POINT('Origin',(2.,8.2,5.));
#10410=CARTESIAN_POINT('Origin',(2.,8.5,5.));
#10411=CARTESIAN_POINT('',(1.5,10.8,5.));
#10412=CARTESIAN_POINT('Origin',(2.,10.8,5.));
#10413=CARTESIAN_POINT('',(1.5,8.5,5.));
#10414=CARTESIAN_POINT('Origin',(2.,10.8,5.));
#11672=UNCERTAINTY_MEASURE_WITH_UNIT(LENGTH_MEASURE(0.001),#11749,
'DISTANCE_ACCURACY_VALUE',
'Maximum model space distance between geometric entities at asserted c
onnectivities');
#11699=UNCERTAINTY_MEASURE_WITH_UNIT(LENGTH_MEASURE(0.001),#11749,
'DISTANCE_ACCURACY_VALUE',
'Maximum model space distance between geometric entities at asserted c
onnectivities');
#11721=(
GEOMETRIC_REPRESENTATION_CONTEXT(3)
GLOBAL_UNCERTAINTY_ASSIGNED_CONTEXT((#11672))
GLOBAL_UNIT_ASSIGNED_CONTEXT((#11749,#11751,#11752))
REPRESENTATION_CONTEXT('','3D')
);
#11748=(
GEOMETRIC_REPRESENTATION_CONTEXT(3)
GLOBAL_UNCERTAINTY_ASSIGNED_CONTEXT((#11699))
GLOBAL_UNIT_ASSIGNED_CONTEXT((#11749,#11751,#11752))
REPRESENTATION_CONTEXT('','3D')
);
#11749=(
LENGTH_UNIT()
NAMED_UNIT(*)
SI_UNIT(.CENTI.,.METRE.)
);
#11751=(
NAMED_UNIT(*)
PLANE_ANGLE_UNIT()
SI_UNIT($,.RADIAN.)
);
#11752=(
NAMED_UNIT(*)
SI_UNIT($,.STERADIAN.)
SOLID_ANGLE_UNIT()
);
#11774=SHAPE_DEFINITION_REPRESENTATION(#11822,#11945);
#11822=PRODUCT_DEFINITION_SHAPE('',$,#11994);
#11945=SHAPE_REPRESENTATION('',(#7054),#11721);
#11972=PRODUCT_DEFINITION_CONTEXT('part definition',#12118,'design');
#11994=PRODUCT_DEFINITION('Dead axle_3','Dead axle (3)',#12042,#11972);
#12042=PRODUCT_DEFINITION_FORMATION('',$,#12141);
#12118=APPLICATION_CONTEXT(
'Core Data for Automotive Mechanical Design Process');
#12119=PRODUCT_CONTEXT('part definition',#12118,'mechanical');
#12141=PRODUCT('Dead axle_3','Dead axle (3)','Dead axle',(#12119));
#12169=PRESENTATION_STYLE_ASSIGNMENT((#12174));
#12174=SURFACE_STYLE_USAGE(.BOTH.,#12179);
#12179=SURFACE_SIDE_STYLE('',(#12184));
#12184=SURFACE_STYLE_FILL_AREA(#12189);
#12189=FILL_AREA_STYLE('CAD Library Painted - Engineering blue',(#12194));
#12194=FILL_AREA_STYLE_COLOUR('CAD Library Painted - Engineering blue',
#12199);
#12199=COLOUR_RGB('CAD Library Painted - Engineering blue',0.12156862745098,
0.356862745098039,0.6);
ENDSEC;
END-ISO-10303-21;
